ISO-10303-21;
HEADER;
FILE_DESCRIPTION (('STEP AP214'),
    '1' );
FILE_NAME ('1.7 Special Key.step',
    '2026-10-06T08:51:13',
    ( '' ),
    ( '' ),
    'SwSTEP 2.0',
    'SolidWorks 2021',
    '' );
FILE_SCHEMA (( 'AUTOMOTIVE_DESIGN' ));
ENDSEC;

DATA;
#559=CYLINDRICAL_SURFACE ( 'NONE', #125629, 9.119999999999999218 ) ;
#1068=DIRECTION ( 'NONE',  ( 0.000000000000000000, 0.000000000000000000, 1.000000000000000000 ) ) ;
#1304=( NAMED_UNIT ( * ) SI_UNIT ( $, .STERADIAN. ) SOLID_ANGLE_UNIT ( ) );
#1993=SHAPE_REPRESENTATION_RELATIONSHIP ( 'NONE' , 'NONE' ,  #108808, #122638 ) ;
#2803=ORIENTED_EDGE ( 'NONE', *, *, #81886, .T. ) ;
#2823=AXIS2_PLACEMENT_3D ( 'NONE', #138707, #69164, #116223 ) ;
#2929=ADVANCED_FACE ( 'NONE', ( #78879 ), #559, .T. ) ;
#4959=CARTESIAN_POINT ( 'NONE',  ( 0.000000000000000000, 0.000000000000000000, 0.000000000000000000 ) ) ;
#6524=VECTOR ( 'NONE', #135837, 1000.000000000000000 ) ;
#7052=CIRCLE ( 'NONE', #25614, 9.119999999999999218 ) ;
#7100=LINE ( 'NONE', #107158, #132505 ) ;
#7940=EDGE_CURVE ( 'NONE', #78254, #98954, #19879, .T. ) ;
#8925=CARTESIAN_POINT ( 'NONE',  ( 0.000000000000000000, 0.000000000000000000, 0.000000000000000000 ) ) ;
#10028=ORIENTED_EDGE ( 'NONE', *, *, #7940, .T. ) ;
#10259=EDGE_CURVE ( 'NONE', #98954, #101163, #123673, .T. ) ;
#10698=DIRECTION ( 'NONE',  ( 0.000000000000000000, 0.000000000000000000, -1.000000000000000000 ) ) ;
#11021=DIRECTION ( 'NONE',  ( -1.000000000000000000, -0.000000000000000000, -0.000000000000000000 ) ) ;
#11391=EDGE_CURVE ( 'NONE', #65367, #36132, #15315, .T. ) ;
#11457=LINE ( 'NONE', #57889, #130716 ) ;
#12352=PRODUCT_DEFINITION_FORMATION_WITH_SPECIFIED_SOURCE ( 'ANY', '', #110337, .NOT_KNOWN. ) ;
#12671=ORIENTED_EDGE ( 'NONE', *, *, #60963, .F. ) ;
#12801=DIRECTION ( 'NONE',  ( 1.000000000000000000, 0.000000000000000000, 0.000000000000000000 ) ) ;
#12964=DIRECTION ( 'NONE',  ( 0.000000000000000000, 0.000000000000000000, -1.000000000000000000 ) ) ;
#13236=VERTEX_POINT ( 'NONE', #78334 ) ;
#13607=PRESENTATION_STYLE_ASSIGNMENT (( #113649 ) ) ;
#14945=DIRECTION ( 'NONE',  ( 0.000000000000000000, 0.000000000000000000, -1.000000000000000000 ) ) ;
#15315=CIRCLE ( 'NONE', #133443, 9.119999999999999218 ) ;
#15372=ORIENTED_EDGE ( 'NONE', *, *, #140821, .T. ) ;
#15506=ORIENTED_EDGE ( 'NONE', *, *, #81886, .F. ) ;
#15757=( GEOMETRIC_REPRESENTATION_CONTEXT ( 3 ) GLOBAL_UNCERTAINTY_ASSIGNED_CONTEXT ( ( #88459 ) ) GLOBAL_UNIT_ASSIGNED_CONTEXT ( ( #123409, #113194, #58170 ) ) REPRESENTATION_CONTEXT ( 'NONE', 'WORKASPACE' ) );
#15847=PLANE ( 'NONE',  #125111 ) ;
#16032=APPLICATION_CONTEXT ( 'automotive_design' ) ;
#16411=AXIS2_PLACEMENT_3D ( 'NONE', #45857, #11021, #111808 ) ;
#17094=CARTESIAN_POINT ( 'NONE',  ( 3.250000000000000000, -5.000000000000000000, -6.123233995736766282E-16 ) ) ;
#17504=ORIENTED_EDGE ( 'NONE', *, *, #140821, .F. ) ;
#17878=VECTOR ( 'NONE', #119416, 1000.000000000000000 ) ;
#18100=ORIENTED_EDGE ( 'NONE', *, *, #11391, .F. ) ;
#18130=AXIS2_PLACEMENT_3D ( 'NONE', #23872, #59379, #12964 ) ;
#18677=LINE ( 'NONE', #29564, #17878 ) ;
#19252=LINE ( 'NONE', #128725, #93725 ) ;
#19879=LINE ( 'NONE', #75716, #132797 ) ;
#19947=UNCERTAINTY_MEASURE_WITH_UNIT (LENGTH_MEASURE( 1.000000000000000082E-05 ), #57177, 'distance_accuracy_value', 'NONE');
#20396=VERTEX_POINT ( 'NONE', #17094 ) ;
#20697=CARTESIAN_POINT ( 'NONE',  ( 3.250000000000000000, 4.999999999999997335, -7.627214432543508948 ) ) ;
#21018=ORIENTED_EDGE ( 'NONE', *, *, #125686, .T. ) ;
#21143=DIRECTION ( 'NONE',  ( -1.000000000000000000, -0.000000000000000000, -0.000000000000000000 ) ) ;
#21330=DIRECTION ( 'NONE',  ( -1.000000000000000000, -0.000000000000000000, -0.000000000000000000 ) ) ;
#21496=ORIENTED_EDGE ( 'NONE', *, *, #26001, .F. ) ;
#21683=ADVANCED_FACE ( 'NONE', ( #79414 ), #22789, .T. ) ;
#22261=ORIENTED_EDGE ( 'NONE', *, *, #60384, .T. ) ;
#22372=PRODUCT_DEFINITION_SHAPE ( 'NONE', 'NONE',  #87323 ) ;
#22593=ADVANCED_FACE ( 'NONE', ( #115172 ), #15847, .F. ) ;
#22789=CYLINDRICAL_SURFACE ( 'NONE', #97138, 9.119999999999999218 ) ;
#23259=VECTOR ( 'NONE', #79401, 1000.000000000000000 ) ;
#23803=FILL_AREA_STYLE_COLOUR ( '', #63104 ) ;
#23872=CARTESIAN_POINT ( 'NONE',  ( 3.250000000000000000, 0.000000000000000000, 0.000000000000000000 ) ) ;
#25242=AXIS2_PLACEMENT_3D ( 'NONE', #134663, #136060, #112879 ) ;
#25376=ORIENTED_EDGE ( 'NONE', *, *, #39059, .T. ) ;
#25568=PRODUCT_DEFINITION_CONTEXT ( 'detailed design', #16032, 'design' ) ;
#25614=AXIS2_PLACEMENT_3D ( 'NONE', #119464, #120917, #10698 ) ;
#26001=EDGE_CURVE ( 'NONE', #20396, #123770, #131342, .T. ) ;
#26033=STYLED_ITEM ( 'NONE', ( #13607 ), #122638 ) ;
#26298=AXIS2_PLACEMENT_3D ( 'NONE', #114329, #127343, #80308 ) ;
#28842=FACE_OUTER_BOUND ( 'NONE', #105895, .T. ) ;
#29564=CARTESIAN_POINT ( 'NONE',  ( 3.250000000000000000, -4.999999999999999112, -7.627214432543508948 ) ) ;
#29815=ORIENTED_EDGE ( 'NONE', *, *, #31125, .F. ) ;
#30546=VERTEX_POINT ( 'NONE', #82064 ) ;
#31125=EDGE_CURVE ( 'NONE', #65367, #88773, #7100, .T. ) ;
#32598=EDGE_CURVE ( 'NONE', #78254, #30546, #54061, .T. ) ;
#32871=ORIENTED_EDGE ( 'NONE', *, *, #118916, .F. ) ;
#34807=ORIENTED_EDGE ( 'NONE', *, *, #44900, .T. ) ;
#34840=EDGE_CURVE ( 'NONE', #13236, #20396, #18677, .T. ) ;
#35596=APPLICATION_CONTEXT ( 'automotive_design' ) ;
#35698=SURFACE_STYLE_USAGE ( .BOTH. , #88627 ) ;
#36132=VERTEX_POINT ( 'NONE', #143375 ) ;
#37045=ORIENTED_EDGE ( 'NONE', *, *, #10259, .F. ) ;
#38360=DIRECTION ( 'NONE',  ( 1.000000000000000000, 0.000000000000000000, 0.000000000000000000 ) ) ;
#38681=EDGE_LOOP ( 'NONE', ( #52025, #18100, #113974, #15372 ) ) ;
#39059=EDGE_CURVE ( 'NONE', #30546, #65367, #88112, .T. ) ;
#40989=EDGE_CURVE ( 'NONE', #45628, #123770, #90215, .T. ) ;
#44851=DIRECTION ( 'NONE',  ( 0.000000000000000000, 0.000000000000000000, 1.000000000000000000 ) ) ;
#44900=EDGE_CURVE ( 'NONE', #13236, #45628, #11457, .T. ) ;
#45628=VERTEX_POINT ( 'NONE', #74142 ) ;
#45857=CARTESIAN_POINT ( 'NONE',  ( 0.000000000000000000, 0.000000000000000000, 0.000000000000000000 ) ) ;
#45967=VECTOR ( 'NONE', #86695, 1000.000000000000000 ) ;
#46058=DIRECTION ( 'NONE',  ( -1.000000000000000000, -0.000000000000000000, -0.000000000000000000 ) ) ;
#46234=FACE_OUTER_BOUND ( 'NONE', #138245, .T. ) ;
#46519=ORIENTED_EDGE ( 'NONE', *, *, #81818, .F. ) ;
#46908=MANIFOLD_SOLID_BREP ( 'Boss-Extrude1', #106478 ) ;
#47733=FILL_AREA_STYLE ('',( #23803 ) ) ;
#49233=MECHANICAL_DESIGN_GEOMETRIC_PRESENTATION_REPRESENTATION('',(#26033),#67779);
#49881=ORIENTED_EDGE ( 'NONE', *, *, #34840, .F. ) ;
#50394=ADVANCED_FACE ( 'NONE', ( #46234 ), #90416, .F. ) ;
#52025=ORIENTED_EDGE ( 'NONE', *, *, #88274, .F. ) ;
#52073=CARTESIAN_POINT ( 'NONE',  ( 3.250000000000000000, 4.999999999999997335, -7.627214432543508948 ) ) ;
#52273=CARTESIAN_POINT ( 'NONE',  ( 3.250000000000000000, 0.000000000000000000, 4.999999999999998224 ) ) ;
#52835=STYLED_ITEM ( 'NONE', ( #122650 ), #46908 ) ;
#53195=DIRECTION ( 'NONE',  ( 1.000000000000000000, 0.000000000000000000, 0.000000000000000000 ) ) ;
#54061=CIRCLE ( 'NONE', #26298, 4.999999999999998224 ) ;
#56241=CYLINDRICAL_SURFACE ( 'NONE', #122685, 4.999999999999998224 ) ;
#57177=( LENGTH_UNIT ( ) NAMED_UNIT ( * ) SI_UNIT ( .MILLI., .METRE. ) );
#57301=CARTESIAN_POINT ( 'NONE',  ( 3.250000000000000000, -4.999999999999999112, -7.627214432543508948 ) ) ;
#57889=CARTESIAN_POINT ( 'NONE',  ( 3.250000000000000000, -4.999999999999999112, -7.627214432543508948 ) ) ;
#57890=SURFACE_STYLE_FILL_AREA ( #47733 ) ;
#58170=( NAMED_UNIT ( * ) SI_UNIT ( $, .STERADIAN. ) SOLID_ANGLE_UNIT ( ) );
#59110=DIRECTION ( 'NONE',  ( -1.000000000000000000, -0.000000000000000000, -0.000000000000000000 ) ) ;
#59379=DIRECTION ( 'NONE',  ( 1.000000000000000000, 0.000000000000000000, 0.000000000000000000 ) ) ;
#59429=DIRECTION ( 'NONE',  ( 0.000000000000000000, 0.000000000000000000, -1.000000000000000000 ) ) ;
#59764=DIRECTION ( 'NONE',  ( 1.000000000000000000, 0.000000000000000000, 0.000000000000000000 ) ) ;
#60144=DIRECTION ( 'NONE',  ( 0.000000000000000000, -1.000000000000000000, -1.137193330093851361E-16 ) ) ;
#60384=EDGE_CURVE ( 'NONE', #123770, #98954, #120620, .T. ) ;
#60963=EDGE_CURVE ( 'NONE', #68120, #45628, #123036, .T. ) ;
#62032=ORIENTED_EDGE ( 'NONE', *, *, #40989, .F. ) ;
#63104=COLOUR_RGB ( '', 0.08235294, 0.09019608, 0.10196078) ;
#63852=CARTESIAN_POINT ( 'NONE',  ( 0.000000000000000000, 4.999999999999997335, -7.627214432543508948 ) ) ;
#64351=CARTESIAN_POINT ( 'NONE',  ( 0.000000000000000000, 4.999999999999997335, -7.627214432543508948 ) ) ;
#64718=FILL_AREA_STYLE_COLOUR ( '', #66840 ) ;
#65367=VERTEX_POINT ( 'NONE', #52073 ) ;
#65375=CIRCLE ( 'NONE', #2823, 4.999999999999998224 ) ;
#65459=DIRECTION ( 'NONE',  ( -1.000000000000000000, -0.000000000000000000, -0.000000000000000000 ) ) ;
#66840=COLOUR_RGB ( '', 0.08235294, 0.09019608, 0.10196078) ;
#67603=SURFACE_STYLE_FILL_AREA ( #87178 ) ;
#67779=( GEOMETRIC_REPRESENTATION_CONTEXT ( 3 ) GLOBAL_UNCERTAINTY_ASSIGNED_CONTEXT ( ( #19947 ) ) GLOBAL_UNIT_ASSIGNED_CONTEXT ( ( #57177, #136118, #1304 ) ) REPRESENTATION_CONTEXT ( 'NONE', 'WORKASPACE' ) );
#68120=VERTEX_POINT ( 'NONE', #70202 ) ;
#68756=DIRECTION ( 'NONE',  ( -1.000000000000000000, -0.000000000000000000, -0.000000000000000000 ) ) ;
#68826=FACE_OUTER_BOUND ( 'NONE', #78333, .T. ) ;
#69164=DIRECTION ( 'NONE',  ( -1.000000000000000000, -0.000000000000000000, -0.000000000000000000 ) ) ;
#69698=EDGE_LOOP ( 'NONE', ( #75848, #32871, #127782, #22261 ) ) ;
#69911=LINE ( 'NONE', #73270, #6524 ) ;
#70202=CARTESIAN_POINT ( 'NONE',  ( 0.000000000000000000, 0.000000000000000000, 9.119999999999999218 ) ) ;
#73270=CARTESIAN_POINT ( 'NONE',  ( 3.250000000000000000, 4.999999999999998224, 8.040613248383180784E-16 ) ) ;
#73766=DIRECTION ( 'NONE',  ( -1.000000000000000000, -0.000000000000000000, -0.000000000000000000 ) ) ;
#73830=DIRECTION ( 'NONE',  ( -1.000000000000000000, -0.000000000000000000, -0.000000000000000000 ) ) ;
#74142=CARTESIAN_POINT ( 'NONE',  ( 0.000000000000000000, -4.999999999999999112, -7.627214432543508948 ) ) ;
#74504=CARTESIAN_POINT ( 'NONE',  ( 3.250000000000000000, 0.000000000000000000, 0.000000000000000000 ) ) ;
#74654=ORIENTED_EDGE ( 'NONE', *, *, #81818, .T. ) ;
#75716=CARTESIAN_POINT ( 'NONE',  ( 3.250000000000000000, 0.000000000000000000, 4.999999999999998224 ) ) ;
#75848=ORIENTED_EDGE ( 'NONE', *, *, #7940, .F. ) ;
#75940=LINE ( 'NONE', #64351, #122833 ) ;
#76178=ORIENTED_EDGE ( 'NONE', *, *, #40989, .T. ) ;
#76616=ORIENTED_EDGE ( 'NONE', *, *, #32598, .T. ) ;
#76884=ORIENTED_EDGE ( 'NONE', *, *, #88274, .T. ) ;
#78093=DIRECTION ( 'NONE',  ( -0.000000000000000000, 1.137193330093850868E-16, -1.000000000000000000 ) ) ;
#78254=VERTEX_POINT ( 'NONE', #52273 ) ;
#78333=EDGE_LOOP ( 'NONE', ( #87940, #2803, #114339, #123849, #76616, #25376 ) ) ;
#78334=CARTESIAN_POINT ( 'NONE',  ( 3.250000000000000000, -4.999999999999999112, -7.627214432543508948 ) ) ;
#78879=FACE_OUTER_BOUND ( 'NONE', #127650, .T. ) ;
#79401=DIRECTION ( 'NONE',  ( 0.000000000000000000, -1.137193330093851115E-16, 1.000000000000000000 ) ) ;
#79414=FACE_OUTER_BOUND ( 'NONE', #38681, .T. ) ;
#80308=DIRECTION ( 'NONE',  ( 0.000000000000000000, 0.000000000000000000, -1.000000000000000000 ) ) ;
#81818=EDGE_CURVE ( 'NONE', #101163, #88773, #75940, .T. ) ;
#81886=EDGE_CURVE ( 'NONE', #36132, #13236, #85771, .T. ) ;
#82064=CARTESIAN_POINT ( 'NONE',  ( 3.250000000000000000, 4.999999999999998224, 8.040613248383180784E-16 ) ) ;
#84484=ORIENTED_EDGE ( 'NONE', *, *, #60963, .T. ) ;
#85771=CIRCLE ( 'NONE', #104275, 9.119999999999999218 ) ;
#85967=DIRECTION ( 'NONE',  ( -0.000000000000000000, 1.000000000000000000, 1.137193330093851115E-16 ) ) ;
#86208=( NAMED_UNIT ( * ) SI_UNIT ( $, .STERADIAN. ) SOLID_ANGLE_UNIT ( ) );
#86695=DIRECTION ( 'NONE',  ( -0.000000000000000000, 1.137193330093850868E-16, -1.000000000000000000 ) ) ;
#86699=PLANE ( 'NONE',  #87746 ) ;
#87178=FILL_AREA_STYLE ('',( #64718 ) ) ;
#87323=PRODUCT_DEFINITION ( 'UNKNOWN', '', #12352, #25568 ) ;
#87486=ORIENTED_EDGE ( 'NONE', *, *, #10259, .T. ) ;
#87746=AXIS2_PLACEMENT_3D ( 'NONE', #20697, #85967, #131624 ) ;
#87832=CARTESIAN_POINT ( 'NONE',  ( 3.250000000000000000, -5.000000000000000000, -6.123233995736766282E-16 ) ) ;
#87940=ORIENTED_EDGE ( 'NONE', *, *, #11391, .T. ) ;
#88112=LINE ( 'NONE', #132361, #45967 ) ;
#88274=EDGE_CURVE ( 'NONE', #36132, #68120, #19252, .T. ) ;
#88459=UNCERTAINTY_MEASURE_WITH_UNIT (LENGTH_MEASURE( 1.000000000000000082E-05 ), #123409, 'distance_accuracy_value', 'NONE');
#88627=SURFACE_SIDE_STYLE ('',( #67603 ) ) ;
#88773=VERTEX_POINT ( 'NONE', #63852 ) ;
#89517=CARTESIAN_POINT ( 'NONE',  ( 3.250000000000000000, 0.000000000000000000, 0.000000000000000000 ) ) ;
#90215=LINE ( 'NONE', #134456, #23259 ) ;
#90416=PLANE ( 'NONE',  #25242 ) ;
#90831=ORIENTED_EDGE ( 'NONE', *, *, #44900, .F. ) ;
#92025=DIRECTION ( 'NONE',  ( 0.000000000000000000, 1.137193330093851361E-16, -1.000000000000000000 ) ) ;
#93088=DIRECTION ( 'NONE',  ( 0.000000000000000000, 0.000000000000000000, -1.000000000000000000 ) ) ;
#93725=VECTOR ( 'NONE', #138906, 1000.000000000000000 ) ;
#95503=CYLINDRICAL_SURFACE ( 'NONE', #111851, 4.999999999999998224 ) ;
#95917=ADVANCED_FACE ( 'NONE', ( #119982 ), #86699, .F. ) ;
#97138=AXIS2_PLACEMENT_3D ( 'NONE', #89517, #122861, #131608 ) ;
#97784=( LENGTH_UNIT ( ) NAMED_UNIT ( * ) SI_UNIT ( .MILLI., .METRE. ) );
#98954=VERTEX_POINT ( 'NONE', #134925 ) ;
#99266=EDGE_LOOP ( 'NONE', ( #76178, #21496, #49881, #34807 ) ) ;
#100421=CARTESIAN_POINT ( 'NONE',  ( 3.250000000000000000, 0.000000000000000000, 0.000000000000000000 ) ) ;
#100647=ADVANCED_FACE ( 'NONE', ( #28842 ), #95503, .F. ) ;
#101163=VERTEX_POINT ( 'NONE', #132294 ) ;
#101834=FACE_OUTER_BOUND ( 'NONE', #69698, .T. ) ;
#104275=AXIS2_PLACEMENT_3D ( 'NONE', #114944, #12801, #14945 ) ;
#105628=CARTESIAN_POINT ( 'NONE',  ( 0.000000000000000000, -5.000000000000000000, -6.123233995736766282E-16 ) ) ;
#105895=EDGE_LOOP ( 'NONE', ( #126770, #10028, #87486, #126584 ) ) ;
#106478=CLOSED_SHELL ( 'NONE', ( #100647, #2929, #21683, #22593, #140206, #95917, #125960, #50394 ) ) ;
#107158=CARTESIAN_POINT ( 'NONE',  ( 3.250000000000000000, 4.999999999999997335, -7.627214432543508948 ) ) ;
#108808=SHAPE_REPRESENTATION ( '1.7 Special Key', ( #127880 ), #114089 ) ;
#110337=PRODUCT ( '1.7 Special Key', '1.7 Special Key', '', ( #136657 ) ) ;
#111515=( NAMED_UNIT ( * ) PLANE_ANGLE_UNIT ( ) SI_UNIT ( $, .RADIAN. ) );
#111808=DIRECTION ( 'NONE',  ( 0.000000000000000000, 0.000000000000000000, -1.000000000000000000 ) ) ;
#111851=AXIS2_PLACEMENT_3D ( 'NONE', #74504, #73766, #141147 ) ;
#112879=DIRECTION ( 'NONE',  ( 0.000000000000000000, 0.000000000000000000, -1.000000000000000000 ) ) ;
#112999=PLANE ( 'NONE',  #18130 ) ;
#113194=( NAMED_UNIT ( * ) PLANE_ANGLE_UNIT ( ) SI_UNIT ( $, .RADIAN. ) );
#113649=SURFACE_STYLE_USAGE ( .BOTH. , #123133 ) ;
#113974=ORIENTED_EDGE ( 'NONE', *, *, #31125, .T. ) ;
#114089=( GEOMETRIC_REPRESENTATION_CONTEXT ( 3 ) GLOBAL_UNCERTAINTY_ASSIGNED_CONTEXT ( ( #121404 ) ) GLOBAL_UNIT_ASSIGNED_CONTEXT ( ( #97784, #111515, #86208 ) ) REPRESENTATION_CONTEXT ( 'NONE', 'WORKASPACE' ) );
#114329=CARTESIAN_POINT ( 'NONE',  ( 3.250000000000000000, 0.000000000000000000, 0.000000000000000000 ) ) ;
#114339=ORIENTED_EDGE ( 'NONE', *, *, #34840, .T. ) ;
#114944=CARTESIAN_POINT ( 'NONE',  ( 3.250000000000000000, 0.000000000000000000, 0.000000000000000000 ) ) ;
#115172=FACE_OUTER_BOUND ( 'NONE', #99266, .T. ) ;
#115493=EDGE_LOOP ( 'NONE', ( #74654, #29815, #116918, #21018 ) ) ;
#116223=DIRECTION ( 'NONE',  ( 0.000000000000000000, 0.000000000000000000, -1.000000000000000000 ) ) ;
#116700=AXIS2_PLACEMENT_3D ( 'NONE', #129238, #65459, #121219 ) ;
#116918=ORIENTED_EDGE ( 'NONE', *, *, #39059, .F. ) ;
#118580=VECTOR ( 'NONE', #21143, 1000.000000000000000 ) ;
#118916=EDGE_CURVE ( 'NONE', #20396, #78254, #65375, .T. ) ;
#119416=DIRECTION ( 'NONE',  ( 0.000000000000000000, -1.137193330093851115E-16, 1.000000000000000000 ) ) ;
#119464=CARTESIAN_POINT ( 'NONE',  ( 0.000000000000000000, 0.000000000000000000, 0.000000000000000000 ) ) ;
#119982=FACE_OUTER_BOUND ( 'NONE', #115493, .T. ) ;
#120620=CIRCLE ( 'NONE', #16411, 4.999999999999998224 ) ;
#120917=DIRECTION ( 'NONE',  ( 1.000000000000000000, 0.000000000000000000, 0.000000000000000000 ) ) ;
#121219=DIRECTION ( 'NONE',  ( 0.000000000000000000, 0.000000000000000000, -1.000000000000000000 ) ) ;
#121404=UNCERTAINTY_MEASURE_WITH_UNIT (LENGTH_MEASURE( 1.000000000000000082E-05 ), #97784, 'distance_accuracy_value', 'NONE');
#122380=MECHANICAL_DESIGN_GEOMETRIC_PRESENTATION_REPRESENTATION('',(#52835),#15757);
#122638=ADVANCED_BREP_SHAPE_REPRESENTATION ( '', ( #46908, #127880 ), #114089 ) ;
#122650=PRESENTATION_STYLE_ASSIGNMENT (( #35698 ) ) ;
#122685=AXIS2_PLACEMENT_3D ( 'NONE', #100421, #46058, #1068 ) ;
#122833=VECTOR ( 'NONE', #78093, 1000.000000000000000 ) ;
#122861=DIRECTION ( 'NONE',  ( -1.000000000000000000, -0.000000000000000000, -0.000000000000000000 ) ) ;
#123036=CIRCLE ( 'NONE', #125309, 9.119999999999999218 ) ;
#123133=SURFACE_SIDE_STYLE ('',( #57890 ) ) ;
#123409=( LENGTH_UNIT ( ) NAMED_UNIT ( * ) SI_UNIT ( .MILLI., .METRE. ) );
#123673=CIRCLE ( 'NONE', #116700, 4.999999999999998224 ) ;
#123770=VERTEX_POINT ( 'NONE', #105628 ) ;
#123849=ORIENTED_EDGE ( 'NONE', *, *, #118916, .T. ) ;
#125111=AXIS2_PLACEMENT_3D ( 'NONE', #57301, #60144, #92025 ) ;
#125309=AXIS2_PLACEMENT_3D ( 'NONE', #4959, #38360, #59429 ) ;
#125629=AXIS2_PLACEMENT_3D ( 'NONE', #133949, #59110, #44851 ) ;
#125686=EDGE_CURVE ( 'NONE', #30546, #101163, #69911, .T. ) ;
#125960=ADVANCED_FACE ( 'NONE', ( #68826 ), #112999, .T. ) ;
#126584=ORIENTED_EDGE ( 'NONE', *, *, #125686, .F. ) ;
#126770=ORIENTED_EDGE ( 'NONE', *, *, #32598, .F. ) ;
#127343=DIRECTION ( 'NONE',  ( -1.000000000000000000, -0.000000000000000000, -0.000000000000000000 ) ) ;
#127650=EDGE_LOOP ( 'NONE', ( #15506, #76884, #84484, #90831 ) ) ;
#127782=ORIENTED_EDGE ( 'NONE', *, *, #26001, .T. ) ;
#127879=CARTESIAN_POINT ( 'NONE',  ( 3.250000000000000000, 0.000000000000000000, 0.000000000000000000 ) ) ;
#127880=AXIS2_PLACEMENT_3D ( 'NONE', #8925, #141658, #53195 ) ;
#127953=SHAPE_DEFINITION_REPRESENTATION ( #22372, #108808 ) ;
#128725=CARTESIAN_POINT ( 'NONE',  ( 3.250000000000000000, 0.000000000000000000, 9.119999999999999218 ) ) ;
#129238=CARTESIAN_POINT ( 'NONE',  ( 0.000000000000000000, 0.000000000000000000, 0.000000000000000000 ) ) ;
#130140=ORIENTED_EDGE ( 'NONE', *, *, #60384, .F. ) ;
#130716=VECTOR ( 'NONE', #68756, 1000.000000000000000 ) ;
#131342=LINE ( 'NONE', #87832, #118580 ) ;
#131608=DIRECTION ( 'NONE',  ( 0.000000000000000000, 0.000000000000000000, 1.000000000000000000 ) ) ;
#131624=DIRECTION ( 'NONE',  ( 0.000000000000000000, -1.137193330093851115E-16, 1.000000000000000000 ) ) ;
#132294=CARTESIAN_POINT ( 'NONE',  ( 0.000000000000000000, 4.999999999999998224, 8.040613248383180784E-16 ) ) ;
#132361=CARTESIAN_POINT ( 'NONE',  ( 3.250000000000000000, 4.999999999999997335, -7.627214432543508948 ) ) ;
#132505=VECTOR ( 'NONE', #73830, 1000.000000000000000 ) ;
#132797=VECTOR ( 'NONE', #21330, 1000.000000000000000 ) ;
#133443=AXIS2_PLACEMENT_3D ( 'NONE', #127879, #59764, #93088 ) ;
#133949=CARTESIAN_POINT ( 'NONE',  ( 3.250000000000000000, 0.000000000000000000, 0.000000000000000000 ) ) ;
#134456=CARTESIAN_POINT ( 'NONE',  ( 0.000000000000000000, -4.999999999999999112, -7.627214432543508948 ) ) ;
#134663=CARTESIAN_POINT ( 'NONE',  ( 0.000000000000000000, 0.000000000000000000, 0.000000000000000000 ) ) ;
#134925=CARTESIAN_POINT ( 'NONE',  ( 0.000000000000000000, 0.000000000000000000, 4.999999999999998224 ) ) ;
#135837=DIRECTION ( 'NONE',  ( -1.000000000000000000, -0.000000000000000000, -0.000000000000000000 ) ) ;
#136060=DIRECTION ( 'NONE',  ( 1.000000000000000000, 0.000000000000000000, 0.000000000000000000 ) ) ;
#136118=( NAMED_UNIT ( * ) PLANE_ANGLE_UNIT ( ) SI_UNIT ( $, .RADIAN. ) );
#136657=PRODUCT_CONTEXT ( 'NONE', #35596, 'mechanical' ) ;
#138245=EDGE_LOOP ( 'NONE', ( #17504, #46519, #37045, #130140, #62032, #12671 ) ) ;
#138707=CARTESIAN_POINT ( 'NONE',  ( 3.250000000000000000, 0.000000000000000000, 0.000000000000000000 ) ) ;
#138906=DIRECTION ( 'NONE',  ( -1.000000000000000000, -0.000000000000000000, -0.000000000000000000 ) ) ;
#140206=ADVANCED_FACE ( 'NONE', ( #101834 ), #56241, .F. ) ;
#140821=EDGE_CURVE ( 'NONE', #88773, #68120, #7052, .T. ) ;
#141147=DIRECTION ( 'NONE',  ( 0.000000000000000000, 0.000000000000000000, 1.000000000000000000 ) ) ;
#141658=DIRECTION ( 'NONE',  ( 0.000000000000000000, 0.000000000000000000, 1.000000000000000000 ) ) ;
#143375=CARTESIAN_POINT ( 'NONE',  ( 3.250000000000000000, 0.000000000000000000, 9.119999999999999218 ) ) ;
ENDSEC;
END-ISO-10303-21;
